ISO-10303-21;
HEADER;
/* Generated by software containing ST-Developer
 * from STEP Tools, Inc. (www.steptools.com) 
 */

FILE_DESCRIPTION(
/* description */ ('Bearing friction torque test rig'),
/* implementation_level */ '2;1');

FILE_NAME(
/* name */ 'Outer journal spacer (1).step',
/* time_stamp */ '2026-10-28T03:24:04-07:00',
/* author */ (''),
/* organization */ (''),
/* preprocessor_version */ 'ST-DEVELOPER v20.2',
/* originating_system */ 'Autodesk Translation Framework v15.17.0.0',
/* authorisation */ '');

FILE_SCHEMA (('AUTOMOTIVE_DESIGN { 1 0 10303 214 3 1 1 }'));
ENDSEC;

DATA;
#10=MECHANICAL_DESIGN_GEOMETRIC_PRESENTATION_REPRESENTATION('',(#588),#14822);
#495=SHAPE_REPRESENTATION_RELATIONSHIP('SRR','None',#15037,#534);
#534=ADVANCED_BREP_SHAPE_REPRESENTATION('',(#639),#14817);
#588=STYLED_ITEM('',(#15277),#639);
#639=MANIFOLD_SOLID_BREP('Body1',#7707);
#850=FACE_BOUND('',#2155,.T.);
#851=FACE_BOUND('',#2157,.T.);
#1075=PLANE('',#9069);
#1076=PLANE('',#9070);
#1501=FACE_OUTER_BOUND('',#2152,.T.);
#1502=FACE_OUTER_BOUND('',#2153,.T.);
#1503=FACE_OUTER_BOUND('',#2154,.T.);
#1504=FACE_OUTER_BOUND('',#2156,.T.);
#2152=EDGE_LOOP('',(#6856,#6857,#6858,#6859));
#2153=EDGE_LOOP('',(#6860,#6861,#6862,#6863));
#2154=EDGE_LOOP('',(#6864));
#2155=EDGE_LOOP('',(#6865));
#2156=EDGE_LOOP('',(#6866));
#2157=EDGE_LOOP('',(#6867));
#2620=LINE('',#14344,#3064);
#2621=LINE('',#14350,#3065);
#3064=VECTOR('',#11413,0.605);
#3065=VECTOR('',#11420,0.9);
#3514=CIRCLE('',#9064,0.605);
#3515=CIRCLE('',#9065,0.605);
#3516=CIRCLE('',#9067,0.9);
#3517=CIRCLE('',#9068,0.9);
#4137=VERTEX_POINT('',#14341);
#4138=VERTEX_POINT('',#14343);
#4139=VERTEX_POINT('',#14347);
#4140=VERTEX_POINT('',#14349);
#5054=EDGE_CURVE('',#4137,#4137,#3514,.T.);
#5055=EDGE_CURVE('',#4137,#4138,#2620,.T.);
#5056=EDGE_CURVE('',#4138,#4138,#3515,.T.);
#5057=EDGE_CURVE('',#4139,#4139,#3516,.T.);
#5058=EDGE_CURVE('',#4139,#4140,#2621,.T.);
#5059=EDGE_CURVE('',#4140,#4140,#3517,.T.);
#6856=ORIENTED_EDGE('',*,*,#5054,.F.);
#6857=ORIENTED_EDGE('',*,*,#5055,.T.);
#6858=ORIENTED_EDGE('',*,*,#5056,.T.);
#6859=ORIENTED_EDGE('',*,*,#5055,.F.);
#6860=ORIENTED_EDGE('',*,*,#5057,.F.);
#6861=ORIENTED_EDGE('',*,*,#5058,.T.);
#6862=ORIENTED_EDGE('',*,*,#5059,.T.);
#6863=ORIENTED_EDGE('',*,*,#5058,.F.);
#6864=ORIENTED_EDGE('',*,*,#5057,.T.);
#6865=ORIENTED_EDGE('',*,*,#5054,.T.);
#6866=ORIENTED_EDGE('',*,*,#5059,.F.);
#6867=ORIENTED_EDGE('',*,*,#5056,.F.);
#7193=CYLINDRICAL_SURFACE('',#9063,0.605);
#7194=CYLINDRICAL_SURFACE('',#9066,0.9);
#7612=ADVANCED_FACE('',(#1501),#7193,.F.);
#7613=ADVANCED_FACE('',(#1502),#7194,.T.);
#7614=ADVANCED_FACE('',(#1503,#850),#1075,.T.);
#7615=ADVANCED_FACE('',(#1504,#851),#1076,.F.);
#7707=CLOSED_SHELL('',(#7612,#7613,#7614,#7615));
#9062=AXIS2_PLACEMENT_3D('',#14339,#11407,#11408);
#9063=AXIS2_PLACEMENT_3D('',#14340,#11409,#11410);
#9064=AXIS2_PLACEMENT_3D('',#14342,#11411,#11412);
#9065=AXIS2_PLACEMENT_3D('',#14345,#11414,#11415);
#9066=AXIS2_PLACEMENT_3D('',#14346,#11416,#11417);
#9067=AXIS2_PLACEMENT_3D('',#14348,#11418,#11419);
#9068=AXIS2_PLACEMENT_3D('',#14351,#11421,#11422);
#9069=AXIS2_PLACEMENT_3D('',#14352,#11423,#11424);
#9070=AXIS2_PLACEMENT_3D('',#14353,#11425,#11426);
#11407=DIRECTION('axis',(0.,0.,1.));
#11408=DIRECTION('refdir',(1.,0.,0.));
#11409=DIRECTION('center_axis',(0.,1.,0.));
#11410=DIRECTION('ref_axis',(1.,0.,0.));
#11411=DIRECTION('center_axis',(0.,-1.,0.));
#11412=DIRECTION('ref_axis',(1.,0.,0.));
#11413=DIRECTION('',(0.,-1.,0.));
#11414=DIRECTION('center_axis',(0.,-1.,0.));
#11415=DIRECTION('ref_axis',(1.,0.,0.));
#11416=DIRECTION('center_axis',(0.,1.,0.));
#11417=DIRECTION('ref_axis',(1.,0.,0.));
#11418=DIRECTION('center_axis',(0.,1.,0.));
#11419=DIRECTION('ref_axis',(1.,0.,0.));
#11420=DIRECTION('',(0.,-1.,0.));
#11421=DIRECTION('center_axis',(0.,1.,0.));
#11422=DIRECTION('ref_axis',(1.,0.,0.));
#11423=DIRECTION('center_axis',(0.,1.,0.));
#11424=DIRECTION('ref_axis',(1.,0.,0.));
#11425=DIRECTION('center_axis',(0.,1.,0.));
#11426=DIRECTION('ref_axis',(1.,0.,0.));
#14339=CARTESIAN_POINT('',(0.,0.,0.));
#14340=CARTESIAN_POINT('Origin',(0.,7.5,7.));
#14341=CARTESIAN_POINT('',(-0.605,8.2,7.));
#14342=CARTESIAN_POINT('Origin',(0.,8.2,7.));
#14343=CARTESIAN_POINT('',(-0.605,7.5,7.));
#14344=CARTESIAN_POINT('',(-0.605,7.5,7.));
#14345=CARTESIAN_POINT('Origin',(0.,7.5,7.));
#14346=CARTESIAN_POINT('Origin',(0.,7.5,7.));
#14347=CARTESIAN_POINT('',(-0.9,8.2,7.));
#14348=CARTESIAN_POINT('Origin',(0.,8.2,7.));
#14349=CARTESIAN_POINT('',(-0.9,7.5,7.));
#14350=CARTESIAN_POINT('',(-0.9,7.5,7.));
#14351=CARTESIAN_POINT('Origin',(0.,7.5,7.));
#14352=CARTESIAN_POINT('Origin',(0.,8.2,7.));
#14353=CARTESIAN_POINT('Origin',(0.,7.5,7.));
#14772=UNCERTAINTY_MEASURE_WITH_UNIT(LENGTH_MEASURE(0.001),#14823,
'DISTANCE_ACCURACY_VALUE',
'Maximum model space distance between geometric entities at asserted c
onnectivities');
#14777=UNCERTAINTY_MEASURE_WITH_UNIT(LENGTH_MEASURE(0.001),#14823,
'DISTANCE_ACCURACY_VALUE',
'Maximum model space distance between geometric entities at asserted c
onnectivities');
#14817=(
GEOMETRIC_REPRESENTATION_CONTEXT(3)
GLOBAL_UNCERTAINTY_ASSIGNED_CONTEXT((#14772))
GLOBAL_UNIT_ASSIGNED_CONTEXT((#14823,#14825,#14826))
REPRESENTATION_CONTEXT('','3D')
);
#14822=(
GEOMETRIC_REPRESENTATION_CONTEXT(3)
GLOBAL_UNCERTAINTY_ASSIGNED_CONTEXT((#14777))
GLOBAL_UNIT_ASSIGNED_CONTEXT((#14823,#14825,#14826))
REPRESENTATION_CONTEXT('','3D')
);
#14823=(
LENGTH_UNIT()
NAMED_UNIT(*)
SI_UNIT(.CENTI.,.METRE.)
);
#14825=(
NAMED_UNIT(*)
PLANE_ANGLE_UNIT()
SI_UNIT($,.RADIAN.)
);
#14826=(
NAMED_UNIT(*)
SI_UNIT($,.STERADIAN.)
SOLID_ANGLE_UNIT()
);
#14866=SHAPE_DEFINITION_REPRESENTATION(#14976,#15037);
#14976=PRODUCT_DEFINITION_SHAPE('',$,#15082);
#15037=SHAPE_REPRESENTATION('',(#9062),#14817);
#15042=PRODUCT_DEFINITION_CONTEXT('part definition',#15176,'design');
#15082=PRODUCT_DEFINITION('Outer journal spacer (1)',
'Outer journal spacer (1)',#15126,#15042);
#15126=PRODUCT_DEFINITION_FORMATION('',$,#15217);
#15176=APPLICATION_CONTEXT(
'Core Data for Automotive Mechanical Design Process');
#15177=PRODUCT_CONTEXT('part definition',#15176,'mechanical');
#15217=PRODUCT('Outer journal spacer (1)','Outer journal spacer (1)',
'Outer journal spacer (1)',(#15177));
#15271=COLOUR_RGB('Sky Blue',0.24,0.69,0.87);
#15272=FILL_AREA_STYLE_COLOUR('',#15271);
#15273=FILL_AREA_STYLE('',(#15272));
#15274=SURFACE_STYLE_FILL_AREA(#15273);
#15275=SURFACE_SIDE_STYLE('',(#15274));
#15276=SURFACE_STYLE_USAGE(.BOTH.,#15275);
#15277=PRESENTATION_STYLE_ASSIGNMENT((#15276));
ENDSEC;
END-ISO-10303-21;
